ISO-10303-21;
HEADER;
/* Generated by software containing ST-Developer
 * from STEP Tools, Inc. (www.steptools.com) 
 */

FILE_DESCRIPTION(
/* description */ ('PAT-003'),
/* implementation_level */ '2;1');

FILE_NAME(
/* name */ 'Hex Bolt - M8x40.step',
/* time_stamp */ '2026-10-29T15:45:40-07:00',
/* author */ (''),
/* organization */ (''),
/* preprocessor_version */ 'ST-DEVELOPER v20.2',
/* originating_system */ 'Autodesk Translation Framework v15.17.0.0',
/* authorisation */ '');

FILE_SCHEMA (('AUTOMOTIVE_DESIGN { 1 0 10303 214 3 1 1 }'));
ENDSEC;

DATA;
#10=MECHANICAL_DESIGN_GEOMETRIC_PRESENTATION_REPRESENTATION('',(#152),#5761);
#87=(
BOUNDED_CURVE()
B_SPLINE_CURVE(2,(#5278,#5279,#5280),.UNSPECIFIED.,.F.,.F.)
B_SPLINE_CURVE_WITH_KNOTS((3,3),(0.14973948338295,0.97160236658079),
 .UNSPECIFIED.)
CURVE()
GEOMETRIC_REPRESENTATION_ITEM()
RATIONAL_B_SPLINE_CURVE((1.07140024848292,1.23714644374248,1.07140024848292))
REPRESENTATION_ITEM('')
);
#88=(
BOUNDED_CURVE()
B_SPLINE_CURVE(2,(#5282,#5283,#5284),.UNSPECIFIED.,.F.,.F.)
B_SPLINE_CURVE_WITH_KNOTS((3,3),(0.14973948338295,0.97160236658079),
 .UNSPECIFIED.)
CURVE()
GEOMETRIC_REPRESENTATION_ITEM()
RATIONAL_B_SPLINE_CURVE((1.07140024848292,1.23714644374248,1.07140024848292))
REPRESENTATION_ITEM('')
);
#89=(
BOUNDED_CURVE()
B_SPLINE_CURVE(2,(#5286,#5287,#5288),.UNSPECIFIED.,.F.,.F.)
B_SPLINE_CURVE_WITH_KNOTS((3,3),(0.14973948338295,0.97160236658079),
 .UNSPECIFIED.)
CURVE()
GEOMETRIC_REPRESENTATION_ITEM()
RATIONAL_B_SPLINE_CURVE((1.07140024848292,1.23714644374248,1.07140024848292))
REPRESENTATION_ITEM('')
);
#90=(
BOUNDED_CURVE()
B_SPLINE_CURVE(2,(#5290,#5291,#5292),.UNSPECIFIED.,.F.,.F.)
B_SPLINE_CURVE_WITH_KNOTS((3,3),(0.149739483382949,0.971602366580789),
 .UNSPECIFIED.)
CURVE()
GEOMETRIC_REPRESENTATION_ITEM()
RATIONAL_B_SPLINE_CURVE((1.07140024848292,1.23714644374248,1.07140024848292))
REPRESENTATION_ITEM('')
);
#91=(
BOUNDED_CURVE()
B_SPLINE_CURVE(2,(#5294,#5295,#5296),.UNSPECIFIED.,.F.,.F.)
B_SPLINE_CURVE_WITH_KNOTS((3,3),(0.14973948338295,0.971602366580789),
 .UNSPECIFIED.)
CURVE()
GEOMETRIC_REPRESENTATION_ITEM()
RATIONAL_B_SPLINE_CURVE((1.07140024848292,1.23714644374248,1.07140024848292))
REPRESENTATION_ITEM('')
);
#92=(
BOUNDED_CURVE()
B_SPLINE_CURVE(2,(#5297,#5298,#5299),.UNSPECIFIED.,.F.,.F.)
B_SPLINE_CURVE_WITH_KNOTS((3,3),(0.14973948338295,0.97160236658079),
 .UNSPECIFIED.)
CURVE()
GEOMETRIC_REPRESENTATION_ITEM()
RATIONAL_B_SPLINE_CURVE((1.07140024848292,1.23714644374248,1.07140024848292))
REPRESENTATION_ITEM('')
);
#113=CONICAL_SURFACE('',#3612,0.36,0.785398163397451);
#114=CONICAL_SURFACE('',#3615,0.734027674973257,1.0471975511966);
#128=SHAPE_REPRESENTATION_RELATIONSHIP('SRR','None',#5822,#140);
#140=ADVANCED_BREP_SHAPE_REPRESENTATION('',(#163),#5753);
#152=STYLED_ITEM('',(#5956),#163);
#163=MANIFOLD_SOLID_BREP('Body1',#3327);
#185=FACE_BOUND('',#655,.T.);
#288=PLANE('',#3614);
#289=PLANE('',#3617);
#290=PLANE('',#3618);
#291=PLANE('',#3619);
#292=PLANE('',#3620);
#293=PLANE('',#3621);
#294=PLANE('',#3622);
#295=PLANE('',#3623);
#296=PLANE('',#3624);
#440=FACE_OUTER_BOUND('',#643,.T.);
#441=FACE_OUTER_BOUND('',#644,.T.);
#442=FACE_OUTER_BOUND('',#645,.T.);
#443=FACE_OUTER_BOUND('',#646,.T.);
#444=FACE_OUTER_BOUND('',#647,.T.);
#445=FACE_OUTER_BOUND('',#648,.T.);
#446=FACE_OUTER_BOUND('',#649,.T.);
#447=FACE_OUTER_BOUND('',#650,.T.);
#448=FACE_OUTER_BOUND('',#651,.T.);
#449=FACE_OUTER_BOUND('',#652,.T.);
#450=FACE_OUTER_BOUND('',#653,.T.);
#451=FACE_OUTER_BOUND('',#654,.T.);
#643=EDGE_LOOP('',(#2708,#2709,#2710,#2711));
#644=EDGE_LOOP('',(#2712,#2713,#2714,#2715));
#645=EDGE_LOOP('',(#2716));
#646=EDGE_LOOP('',(#2717,#2718,#2719,#2720,#2721,#2722,#2723,#2724,#2725));
#647=EDGE_LOOP('',(#2726,#2727,#2728,#2729));
#648=EDGE_LOOP('',(#2730,#2731,#2732,#2733));
#649=EDGE_LOOP('',(#2734,#2735,#2736,#2737));
#650=EDGE_LOOP('',(#2738,#2739,#2740,#2741));
#651=EDGE_LOOP('',(#2742,#2743,#2744,#2745));
#652=EDGE_LOOP('',(#2746,#2747,#2748,#2749));
#653=EDGE_LOOP('',(#2750));
#654=EDGE_LOOP('',(#2751,#2752,#2753,#2754,#2755,#2756));
#655=EDGE_LOOP('',(#2757));
#963=LINE('',#5265,#1285);
#964=LINE('',#5270,#1286);
#965=LINE('',#5276,#1287);
#966=LINE('',#5302,#1288);
#967=LINE('',#5304,#1289);
#968=LINE('',#5305,#1290);
#969=LINE('',#5308,#1291);
#970=LINE('',#5309,#1292);
#971=LINE('',#5312,#1293);
#972=LINE('',#5313,#1294);
#973=LINE('',#5316,#1295);
#974=LINE('',#5317,#1296);
#975=LINE('',#5320,#1297);
#976=LINE('',#5321,#1298);
#977=LINE('',#5323,#1299);
#1285=VECTOR('',#4284,0.4);
#1286=VECTOR('',#4291,0.36);
#1287=VECTOR('',#4298,0.734027674973257);
#1288=VECTOR('',#4301,1.);
#1289=VECTOR('',#4302,1.);
#1290=VECTOR('',#4303,1.);
#1291=VECTOR('',#4306,1.);
#1292=VECTOR('',#4307,1.);
#1293=VECTOR('',#4310,1.);
#1294=VECTOR('',#4311,1.);
#1295=VECTOR('',#4314,1.);
#1296=VECTOR('',#4315,1.);
#1297=VECTOR('',#4318,1.);
#1298=VECTOR('',#4319,1.);
#1299=VECTOR('',#4322,1.);
#1428=CIRCLE('',#3610,0.3933);
#1429=CIRCLE('',#3611,0.3933);
#1430=CIRCLE('',#3613,0.32);
#1431=CIRCLE('',#3616,0.6175);
#1654=VERTEX_POINT('',#5262);
#1655=VERTEX_POINT('',#5264);
#1656=VERTEX_POINT('',#5268);
#1657=VERTEX_POINT('',#5273);
#1658=VERTEX_POINT('',#5275);
#1659=VERTEX_POINT('',#5277);
#1660=VERTEX_POINT('',#5281);
#1661=VERTEX_POINT('',#5285);
#1662=VERTEX_POINT('',#5289);
#1663=VERTEX_POINT('',#5293);
#1664=VERTEX_POINT('',#5301);
#1665=VERTEX_POINT('',#5303);
#1666=VERTEX_POINT('',#5307);
#1667=VERTEX_POINT('',#5311);
#1668=VERTEX_POINT('',#5315);
#1669=VERTEX_POINT('',#5319);
#2025=EDGE_CURVE('',#1654,#1654,#1428,.F.);
#2026=EDGE_CURVE('',#1654,#1655,#963,.T.);
#2027=EDGE_CURVE('',#1655,#1655,#1429,.F.);
#2028=EDGE_CURVE('',#1656,#1656,#1430,.T.);
#2029=EDGE_CURVE('',#1656,#1654,#964,.T.);
#2030=EDGE_CURVE('',#1657,#1657,#1431,.T.);
#2031=EDGE_CURVE('',#1657,#1658,#965,.T.);
#2032=EDGE_CURVE('',#1659,#1658,#87,.T.);
#2033=EDGE_CURVE('',#1660,#1659,#88,.T.);
#2034=EDGE_CURVE('',#1661,#1660,#89,.T.);
#2035=EDGE_CURVE('',#1662,#1661,#90,.T.);
#2036=EDGE_CURVE('',#1663,#1662,#91,.T.);
#2037=EDGE_CURVE('',#1658,#1663,#92,.T.);
#2038=EDGE_CURVE('',#1664,#1662,#966,.T.);
#2039=EDGE_CURVE('',#1664,#1665,#967,.T.);
#2040=EDGE_CURVE('',#1665,#1663,#968,.T.);
#2041=EDGE_CURVE('',#1666,#1661,#969,.T.);
#2042=EDGE_CURVE('',#1666,#1664,#970,.T.);
#2043=EDGE_CURVE('',#1667,#1660,#971,.T.);
#2044=EDGE_CURVE('',#1667,#1666,#972,.T.);
#2045=EDGE_CURVE('',#1668,#1659,#973,.T.);
#2046=EDGE_CURVE('',#1668,#1667,#974,.T.);
#2047=EDGE_CURVE('',#1669,#1658,#975,.T.);
#2048=EDGE_CURVE('',#1669,#1668,#976,.T.);
#2049=EDGE_CURVE('',#1665,#1669,#977,.T.);
#2708=ORIENTED_EDGE('',*,*,#2025,.F.);
#2709=ORIENTED_EDGE('',*,*,#2026,.T.);
#2710=ORIENTED_EDGE('',*,*,#2027,.F.);
#2711=ORIENTED_EDGE('',*,*,#2026,.F.);
#2712=ORIENTED_EDGE('',*,*,#2028,.F.);
#2713=ORIENTED_EDGE('',*,*,#2029,.T.);
#2714=ORIENTED_EDGE('',*,*,#2025,.T.);
#2715=ORIENTED_EDGE('',*,*,#2029,.F.);
#2716=ORIENTED_EDGE('',*,*,#2028,.T.);
#2717=ORIENTED_EDGE('',*,*,#2030,.F.);
#2718=ORIENTED_EDGE('',*,*,#2031,.T.);
#2719=ORIENTED_EDGE('',*,*,#2032,.F.);
#2720=ORIENTED_EDGE('',*,*,#2033,.F.);
#2721=ORIENTED_EDGE('',*,*,#2034,.F.);
#2722=ORIENTED_EDGE('',*,*,#2035,.F.);
#2723=ORIENTED_EDGE('',*,*,#2036,.F.);
#2724=ORIENTED_EDGE('',*,*,#2037,.F.);
#2725=ORIENTED_EDGE('',*,*,#2031,.F.);
#2726=ORIENTED_EDGE('',*,*,#2036,.T.);
#2727=ORIENTED_EDGE('',*,*,#2038,.F.);
#2728=ORIENTED_EDGE('',*,*,#2039,.T.);
#2729=ORIENTED_EDGE('',*,*,#2040,.T.);
#2730=ORIENTED_EDGE('',*,*,#2035,.T.);
#2731=ORIENTED_EDGE('',*,*,#2041,.F.);
#2732=ORIENTED_EDGE('',*,*,#2042,.T.);
#2733=ORIENTED_EDGE('',*,*,#2038,.T.);
#2734=ORIENTED_EDGE('',*,*,#2034,.T.);
#2735=ORIENTED_EDGE('',*,*,#2043,.F.);
#2736=ORIENTED_EDGE('',*,*,#2044,.T.);
#2737=ORIENTED_EDGE('',*,*,#2041,.T.);
#2738=ORIENTED_EDGE('',*,*,#2033,.T.);
#2739=ORIENTED_EDGE('',*,*,#2045,.F.);
#2740=ORIENTED_EDGE('',*,*,#2046,.T.);
#2741=ORIENTED_EDGE('',*,*,#2043,.T.);
#2742=ORIENTED_EDGE('',*,*,#2032,.T.);
#2743=ORIENTED_EDGE('',*,*,#2047,.F.);
#2744=ORIENTED_EDGE('',*,*,#2048,.T.);
#2745=ORIENTED_EDGE('',*,*,#2045,.T.);
#2746=ORIENTED_EDGE('',*,*,#2037,.T.);
#2747=ORIENTED_EDGE('',*,*,#2040,.F.);
#2748=ORIENTED_EDGE('',*,*,#2049,.T.);
#2749=ORIENTED_EDGE('',*,*,#2047,.T.);
#2750=ORIENTED_EDGE('',*,*,#2030,.T.);
#2751=ORIENTED_EDGE('',*,*,#2044,.F.);
#2752=ORIENTED_EDGE('',*,*,#2046,.F.);
#2753=ORIENTED_EDGE('',*,*,#2048,.F.);
#2754=ORIENTED_EDGE('',*,*,#2049,.F.);
#2755=ORIENTED_EDGE('',*,*,#2039,.F.);
#2756=ORIENTED_EDGE('',*,*,#2042,.F.);
#2757=ORIENTED_EDGE('',*,*,#2027,.T.);
#3107=CYLINDRICAL_SURFACE('',#3609,0.3933);
#3233=ADVANCED_FACE('',(#440),#3107,.T.);
#3234=ADVANCED_FACE('',(#441),#113,.T.);
#3235=ADVANCED_FACE('',(#442),#288,.T.);
#3236=ADVANCED_FACE('',(#443),#114,.T.);
#3237=ADVANCED_FACE('',(#444),#289,.T.);
#3238=ADVANCED_FACE('',(#445),#290,.T.);
#3239=ADVANCED_FACE('',(#446),#291,.T.);
#3240=ADVANCED_FACE('',(#447),#292,.T.);
#3241=ADVANCED_FACE('',(#448),#293,.T.);
#3242=ADVANCED_FACE('',(#449),#294,.T.);
#3243=ADVANCED_FACE('',(#450),#295,.T.);
#3244=ADVANCED_FACE('',(#451,#185),#296,.F.);
#3327=CLOSED_SHELL('',(#3233,#3234,#3235,#3236,#3237,#3238,#3239,#3240,
#3241,#3242,#3243,#3244));
#3608=AXIS2_PLACEMENT_3D('',#5260,#4278,#4279);
#3609=AXIS2_PLACEMENT_3D('',#5261,#4280,#4281);
#3610=AXIS2_PLACEMENT_3D('',#5263,#4282,#4283);
#3611=AXIS2_PLACEMENT_3D('',#5266,#4285,#4286);
#3612=AXIS2_PLACEMENT_3D('',#5267,#4287,#4288);
#3613=AXIS2_PLACEMENT_3D('',#5269,#4289,#4290);
#3614=AXIS2_PLACEMENT_3D('',#5271,#4292,#4293);
#3615=AXIS2_PLACEMENT_3D('',#5272,#4294,#4295);
#3616=AXIS2_PLACEMENT_3D('',#5274,#4296,#4297);
#3617=AXIS2_PLACEMENT_3D('',#5300,#4299,#4300);
#3618=AXIS2_PLACEMENT_3D('',#5306,#4304,#4305);
#3619=AXIS2_PLACEMENT_3D('',#5310,#4308,#4309);
#3620=AXIS2_PLACEMENT_3D('',#5314,#4312,#4313);
#3621=AXIS2_PLACEMENT_3D('',#5318,#4316,#4317);
#3622=AXIS2_PLACEMENT_3D('',#5322,#4320,#4321);
#3623=AXIS2_PLACEMENT_3D('',#5324,#4323,#4324);
#3624=AXIS2_PLACEMENT_3D('',#5325,#4325,#4326);
#4278=DIRECTION('axis',(0.,0.,1.));
#4279=DIRECTION('refdir',(1.,0.,0.));
#4280=DIRECTION('center_axis',(0.,-1.,0.));
#4281=DIRECTION('ref_axis',(1.,0.,0.));
#4282=DIRECTION('center_axis',(0.,1.,0.));
#4283=DIRECTION('ref_axis',(1.,0.,0.));
#4284=DIRECTION('',(0.,1.,0.));
#4285=DIRECTION('center_axis',(0.,-1.,0.));
#4286=DIRECTION('ref_axis',(1.,0.,0.));
#4287=DIRECTION('center_axis',(0.,1.,0.));
#4288=DIRECTION('ref_axis',(1.,0.,0.));
#4289=DIRECTION('center_axis',(0.,-1.,0.));
#4290=DIRECTION('ref_axis',(1.,0.,0.));
#4291=DIRECTION('',(-0.707106781186549,0.707106781186546,-8.65956056235496E-17));
#4292=DIRECTION('center_axis',(0.,-1.,0.));
#4293=DIRECTION('ref_axis',(0.,0.,-1.));
#4294=DIRECTION('center_axis',(0.,-1.,0.));
#4295=DIRECTION('ref_axis',(1.,0.,0.));
#4296=DIRECTION('center_axis',(0.,1.,0.));
#4297=DIRECTION('ref_axis',(1.,0.,0.));
#4298=DIRECTION('',(-0.866025403784439,-0.5,-1.06057523872491E-16));
#4299=DIRECTION('center_axis',(1.4792020664489E-16,0.,-1.));
#4300=DIRECTION('ref_axis',(-1.,0.,-1.4792020664489E-16));
#4301=DIRECTION('',(0.,1.,0.));
#4302=DIRECTION('',(-1.,0.,-1.4792020664489E-16));
#4303=DIRECTION('',(0.,1.,0.));
#4304=DIRECTION('center_axis',(0.866025403784439,0.,-0.5));
#4305=DIRECTION('ref_axis',(-0.5,0.,-0.866025403784439));
#4306=DIRECTION('',(0.,1.,0.));
#4307=DIRECTION('',(-0.5,0.,-0.866025403784439));
#4308=DIRECTION('center_axis',(0.866025403784439,0.,0.5));
#4309=DIRECTION('ref_axis',(0.5,0.,-0.866025403784439));
#4310=DIRECTION('',(0.,1.,0.));
#4311=DIRECTION('',(0.5,0.,-0.866025403784439));
#4312=DIRECTION('center_axis',(-2.95840413289779E-16,0.,1.));
#4313=DIRECTION('ref_axis',(1.,0.,2.95840413289779E-16));
#4314=DIRECTION('',(0.,1.,0.));
#4315=DIRECTION('',(1.,0.,2.95840413289779E-16));
#4316=DIRECTION('center_axis',(-0.866025403784439,0.,0.5));
#4317=DIRECTION('ref_axis',(0.5,0.,0.866025403784439));
#4318=DIRECTION('',(0.,1.,0.));
#4319=DIRECTION('',(0.5,0.,0.866025403784439));
#4320=DIRECTION('center_axis',(-0.866025403784439,0.,-0.5));
#4321=DIRECTION('ref_axis',(-0.5,0.,0.866025403784439));
#4322=DIRECTION('',(-0.5,0.,0.866025403784439));
#4323=DIRECTION('center_axis',(0.,1.,0.));
#4324=DIRECTION('ref_axis',(0.,0.,1.));
#4325=DIRECTION('center_axis',(0.,1.,0.));
#4326=DIRECTION('ref_axis',(1.,0.,0.));
#5260=CARTESIAN_POINT('',(0.,0.,0.));
#5261=CARTESIAN_POINT('Origin',(0.,-1.935,0.));
#5262=CARTESIAN_POINT('',(-0.3933,-3.9267,4.81653586104654E-17));
#5263=CARTESIAN_POINT('Origin',(0.,-3.9267,0.));
#5264=CARTESIAN_POINT('',(-0.3933,0.,-4.81653586104654E-17));
#5265=CARTESIAN_POINT('',(-0.3933,-1.935,-4.81653586104654E-17));
#5266=CARTESIAN_POINT('Origin',(0.,0.,0.));
#5267=CARTESIAN_POINT('Origin',(0.,-3.96,0.));
#5268=CARTESIAN_POINT('',(-0.32,-4.,-3.91886975727153E-17));
#5269=CARTESIAN_POINT('Origin',(0.,-4.,0.));
#5270=CARTESIAN_POINT('',(-0.36,-3.96,-4.40872847693047E-17));
#5271=CARTESIAN_POINT('Origin',(0.,-4.,0.));
#5272=CARTESIAN_POINT('Origin',(0.,0.462722715486149,0.));
#5273=CARTESIAN_POINT('',(-0.6175,0.53,-7.5621939847349E-17));
#5274=CARTESIAN_POINT('Origin',(0.,0.53,0.));
#5275=CARTESIAN_POINT('',(-0.750555349946514,0.453180457891261,-9.19165206894919E-17));
#5276=CARTESIAN_POINT('',(-0.734027674973257,0.462722715486149,-8.98924642641573E-17));
#5277=CARTESIAN_POINT('',(-0.375277674973257,0.453180457891261,0.65));
#5278=CARTESIAN_POINT('Ctrl Pts',(-0.375277674973257,0.45318045789126,0.65));
#5279=CARTESIAN_POINT('Ctrl Pts',(-0.562916512459968,0.561513791224244,
0.324999999999856));
#5280=CARTESIAN_POINT('Ctrl Pts',(-0.750555349946514,0.45318045789126,-9.19165206894919E-17));
#5281=CARTESIAN_POINT('',(0.375277674973257,0.453180457891261,0.65));
#5282=CARTESIAN_POINT('Ctrl Pts',(0.375277674973257,0.453180457891261,0.65));
#5283=CARTESIAN_POINT('Ctrl Pts',(-1.66922031752392E-13,0.561513791224244,
0.65));
#5284=CARTESIAN_POINT('Ctrl Pts',(-0.375277674973257,0.45318045789126,0.65));
#5285=CARTESIAN_POINT('',(0.750555349946514,0.453180457891261,0.));
#5286=CARTESIAN_POINT('Ctrl Pts',(0.750555349946514,0.453180457891261,0.));
#5287=CARTESIAN_POINT('Ctrl Pts',(0.562916512459802,0.561513791224244,0.325000000000144));
#5288=CARTESIAN_POINT('Ctrl Pts',(0.375277674973257,0.45318045789126,0.65));
#5289=CARTESIAN_POINT('',(0.375277674973257,0.453180457891261,-0.65));
#5290=CARTESIAN_POINT('Ctrl Pts',(0.375277674973257,0.45318045789126,-0.65));
#5291=CARTESIAN_POINT('Ctrl Pts',(0.562916512459968,0.561513791224244,-0.324999999999855));
#5292=CARTESIAN_POINT('Ctrl Pts',(0.750555349946514,0.453180457891261,0.));
#5293=CARTESIAN_POINT('',(-0.375277674973257,0.45318045789126,-0.65));
#5294=CARTESIAN_POINT('Ctrl Pts',(-0.375277674973257,0.453180457891261,
-0.65));
#5295=CARTESIAN_POINT('Ctrl Pts',(1.66866520601161E-13,0.561513791224244,
-0.65));
#5296=CARTESIAN_POINT('Ctrl Pts',(0.375277674973257,0.45318045789126,-0.65));
#5297=CARTESIAN_POINT('Ctrl Pts',(-0.750555349946514,0.453180457891261,
-9.19165206894919E-17));
#5298=CARTESIAN_POINT('Ctrl Pts',(-0.562916512459802,0.561513791224244,
-0.325000000000144));
#5299=CARTESIAN_POINT('Ctrl Pts',(-0.375277674973257,0.45318045789126,-0.65));
#5300=CARTESIAN_POINT('Origin',(0.375277674973257,0.,-0.65));
#5301=CARTESIAN_POINT('',(0.375277674973257,0.,-0.65));
#5302=CARTESIAN_POINT('',(0.375277674973257,0.,-0.65));
#5303=CARTESIAN_POINT('',(-0.375277674973257,0.,-0.65));
#5304=CARTESIAN_POINT('',(0.375277674973257,0.,-0.65));
#5305=CARTESIAN_POINT('',(-0.375277674973257,0.,-0.65));
#5306=CARTESIAN_POINT('Origin',(0.750555349946514,0.,0.));
#5307=CARTESIAN_POINT('',(0.750555349946514,0.,0.));
#5308=CARTESIAN_POINT('',(0.750555349946514,0.,0.));
#5309=CARTESIAN_POINT('',(0.750555349946514,0.,0.));
#5310=CARTESIAN_POINT('Origin',(0.375277674973257,0.,0.65));
#5311=CARTESIAN_POINT('',(0.375277674973257,0.,0.65));
#5312=CARTESIAN_POINT('',(0.375277674973257,0.,0.65));
#5313=CARTESIAN_POINT('',(0.375277674973257,0.,0.65));
#5314=CARTESIAN_POINT('Origin',(-0.375277674973257,0.,0.65));
#5315=CARTESIAN_POINT('',(-0.375277674973257,0.,0.65));
#5316=CARTESIAN_POINT('',(-0.375277674973257,0.,0.65));
#5317=CARTESIAN_POINT('',(-0.375277674973257,0.,0.65));
#5318=CARTESIAN_POINT('Origin',(-0.750555349946514,0.,-9.19165206894919E-17));
#5319=CARTESIAN_POINT('',(-0.750555349946514,0.,-9.19165206894919E-17));
#5320=CARTESIAN_POINT('',(-0.750555349946514,0.,-9.19165206894919E-17));
#5321=CARTESIAN_POINT('',(-0.750555349946514,0.,-9.19165206894919E-17));
#5322=CARTESIAN_POINT('Origin',(-0.375277674973257,0.,-0.65));
#5323=CARTESIAN_POINT('',(-0.375277674973257,0.,-0.65));
#5324=CARTESIAN_POINT('Origin',(0.,0.53,-1.11022302462516E-16));
#5325=CARTESIAN_POINT('Origin',(0.,0.,-1.11022302462516E-16));
#5737=UNCERTAINTY_MEASURE_WITH_UNIT(LENGTH_MEASURE(0.001),#5762,
'DISTANCE_ACCURACY_VALUE',
'Maximum model space distance between geometric entities at asserted c
onnectivities');
#5745=UNCERTAINTY_MEASURE_WITH_UNIT(LENGTH_MEASURE(0.001),#5762,
'DISTANCE_ACCURACY_VALUE',
'Maximum model space distance between geometric entities at asserted c
onnectivities');
#5753=(
GEOMETRIC_REPRESENTATION_CONTEXT(3)
GLOBAL_UNCERTAINTY_ASSIGNED_CONTEXT((#5737))
GLOBAL_UNIT_ASSIGNED_CONTEXT((#5762,#5764,#5765))
REPRESENTATION_CONTEXT('','3D')
);
#5761=(
GEOMETRIC_REPRESENTATION_CONTEXT(3)
GLOBAL_UNCERTAINTY_ASSIGNED_CONTEXT((#5745))
GLOBAL_UNIT_ASSIGNED_CONTEXT((#5762,#5764,#5765))
REPRESENTATION_CONTEXT('','3D')
);
#5762=(
LENGTH_UNIT()
NAMED_UNIT(*)
SI_UNIT(.CENTI.,.METRE.)
);
#5764=(
NAMED_UNIT(*)
PLANE_ANGLE_UNIT()
SI_UNIT($,.RADIAN.)
);
#5765=(
NAMED_UNIT(*)
SI_UNIT($,.STERADIAN.)
SOLID_ANGLE_UNIT()
);
#5773=SHAPE_DEFINITION_REPRESENTATION(#5788,#5822);
#5788=PRODUCT_DEFINITION_SHAPE('',$,#5838);
#5822=SHAPE_REPRESENTATION('',(#3608),#5753);
#5830=PRODUCT_DEFINITION_CONTEXT('part definition',#5877,'design');
#5838=PRODUCT_DEFINITION('Hex Bolt - M8x40','Hex Bolt - M8x40',#5853,#5830);
#5853=PRODUCT_DEFINITION_FORMATION('',$,#5886);
#5877=APPLICATION_CONTEXT(
'Core Data for Automotive Mechanical Design Process');
#5878=PRODUCT_CONTEXT('part definition',#5877,'mechanical');
#5886=PRODUCT('Hex Bolt - M8x40','Hex Bolt - M8x40','Hex Bolt - M8x40',
(#5878));
#5950=COLOUR_RGB('Black',0.12,0.14,0.17);
#5951=FILL_AREA_STYLE_COLOUR('',#5950);
#5952=FILL_AREA_STYLE('',(#5951));
#5953=SURFACE_STYLE_FILL_AREA(#5952);
#5954=SURFACE_SIDE_STYLE('',(#5953));
#5955=SURFACE_STYLE_USAGE(.BOTH.,#5954);
#5956=PRESENTATION_STYLE_ASSIGNMENT((#5955));
ENDSEC;
END-ISO-10303-21;
